ISO-10303-21;
HEADER;
/* Generated by software containing ST-Developer
 * from STEP Tools, Inc. (www.steptools.com) 
 */

FILE_DESCRIPTION(
/* description */ ('Manifold and mounting hardware'),
/* implementation_level */ '2;1');

FILE_NAME(
/* name */ 'Flat Washer - M6.step',
/* time_stamp */ '2026-10-28T21:46:49-07:00',
/* author */ (''),
/* organization */ (''),
/* preprocessor_version */ 'ST-DEVELOPER v20.2',
/* originating_system */ 'Autodesk Translation Framework v15.17.0.0',
/* authorisation */ '');

FILE_SCHEMA (('AUTOMOTIVE_DESIGN { 1 0 10303 214 3 1 1 }'));
ENDSEC;

DATA;
#10=MECHANICAL_DESIGN_GEOMETRIC_PRESENTATION_REPRESENTATION('',(#162),#5638);
#134=SHAPE_REPRESENTATION_RELATIONSHIP('SRR','None',#5714,#148);
#148=ADVANCED_BREP_SHAPE_REPRESENTATION('',(#176),#5636);
#162=STYLED_ITEM('',(#5867),#176);
#176=MANIFOLD_SOLID_BREP('Body1',#3152);
#250=FACE_BOUND('',#761,.T.);
#251=FACE_BOUND('',#763,.T.);
#327=CYLINDRICAL_SURFACE('',#3624,0.32);
#328=CYLINDRICAL_SURFACE('',#3627,0.6);
#500=FACE_OUTER_BOUND('',#758,.T.);
#501=FACE_OUTER_BOUND('',#759,.T.);
#502=FACE_OUTER_BOUND('',#760,.T.);
#503=FACE_OUTER_BOUND('',#762,.T.);
#758=EDGE_LOOP('',(#2768,#2769,#2770,#2771));
#759=EDGE_LOOP('',(#2772,#2773,#2774,#2775));
#760=EDGE_LOOP('',(#2776));
#761=EDGE_LOOP('',(#2777));
#762=EDGE_LOOP('',(#2778));
#763=EDGE_LOOP('',(#2779));
#889=CIRCLE('',#3625,0.32);
#890=CIRCLE('',#3626,0.32);
#891=CIRCLE('',#3628,0.6);
#892=CIRCLE('',#3629,0.6);
#1127=LINE('',#5506,#1374);
#1128=LINE('',#5512,#1375);
#1374=VECTOR('',#4536,0.32);
#1375=VECTOR('',#4543,0.6);
#1631=VERTEX_POINT('',#5503);
#1632=VERTEX_POINT('',#5505);
#1633=VERTEX_POINT('',#5509);
#1634=VERTEX_POINT('',#5511);
#2013=EDGE_CURVE('',#1631,#1631,#889,.T.);
#2014=EDGE_CURVE('',#1631,#1632,#1127,.T.);
#2015=EDGE_CURVE('',#1632,#1632,#890,.T.);
#2016=EDGE_CURVE('',#1633,#1633,#891,.T.);
#2017=EDGE_CURVE('',#1633,#1634,#1128,.T.);
#2018=EDGE_CURVE('',#1634,#1634,#892,.T.);
#2768=ORIENTED_EDGE('',*,*,#2013,.F.);
#2769=ORIENTED_EDGE('',*,*,#2014,.T.);
#2770=ORIENTED_EDGE('',*,*,#2015,.T.);
#2771=ORIENTED_EDGE('',*,*,#2014,.F.);
#2772=ORIENTED_EDGE('',*,*,#2016,.F.);
#2773=ORIENTED_EDGE('',*,*,#2017,.T.);
#2774=ORIENTED_EDGE('',*,*,#2018,.T.);
#2775=ORIENTED_EDGE('',*,*,#2017,.F.);
#2776=ORIENTED_EDGE('',*,*,#2016,.T.);
#2777=ORIENTED_EDGE('',*,*,#2013,.T.);
#2778=ORIENTED_EDGE('',*,*,#2018,.F.);
#2779=ORIENTED_EDGE('',*,*,#2015,.F.);
#2943=PLANE('',#3630);
#2944=PLANE('',#3631);
#3124=ADVANCED_FACE('',(#500),#327,.F.);
#3125=ADVANCED_FACE('',(#501),#328,.T.);
#3126=ADVANCED_FACE('',(#502,#250),#2943,.T.);
#3127=ADVANCED_FACE('',(#503,#251),#2944,.F.);
#3152=CLOSED_SHELL('',(#3124,#3125,#3126,#3127));
#3623=AXIS2_PLACEMENT_3D('',#5501,#4530,#4531);
#3624=AXIS2_PLACEMENT_3D('',#5502,#4532,#4533);
#3625=AXIS2_PLACEMENT_3D('',#5504,#4534,#4535);
#3626=AXIS2_PLACEMENT_3D('',#5507,#4537,#4538);
#3627=AXIS2_PLACEMENT_3D('',#5508,#4539,#4540);
#3628=AXIS2_PLACEMENT_3D('',#5510,#4541,#4542);
#3629=AXIS2_PLACEMENT_3D('',#5513,#4544,#4545);
#3630=AXIS2_PLACEMENT_3D('',#5514,#4546,#4547);
#3631=AXIS2_PLACEMENT_3D('',#5515,#4548,#4549);
#4530=DIRECTION('axis',(0.,0.,1.));
#4531=DIRECTION('refdir',(1.,0.,0.));
#4532=DIRECTION('center_axis',(0.,1.,0.));
#4533=DIRECTION('ref_axis',(1.,0.,0.));
#4534=DIRECTION('center_axis',(0.,-1.,0.));
#4535=DIRECTION('ref_axis',(1.,0.,0.));
#4536=DIRECTION('',(0.,-1.,0.));
#4537=DIRECTION('center_axis',(0.,-1.,0.));
#4538=DIRECTION('ref_axis',(1.,0.,0.));
#4539=DIRECTION('center_axis',(0.,1.,0.));
#4540=DIRECTION('ref_axis',(1.,0.,0.));
#4541=DIRECTION('center_axis',(0.,1.,0.));
#4542=DIRECTION('ref_axis',(1.,0.,0.));
#4543=DIRECTION('',(0.,-1.,0.));
#4544=DIRECTION('center_axis',(0.,1.,0.));
#4545=DIRECTION('ref_axis',(1.,0.,0.));
#4546=DIRECTION('center_axis',(0.,1.,0.));
#4547=DIRECTION('ref_axis',(1.,0.,0.));
#4548=DIRECTION('center_axis',(0.,1.,0.));
#4549=DIRECTION('ref_axis',(1.,0.,0.));
#5501=CARTESIAN_POINT('',(0.,0.,0.));
#5502=CARTESIAN_POINT('Origin',(0.,0.,0.));
#5503=CARTESIAN_POINT('',(-0.32,0.16,3.91886975727153E-17));
#5504=CARTESIAN_POINT('Origin',(0.,0.16,0.));
#5505=CARTESIAN_POINT('',(-0.32,0.,3.91886975727153E-17));
#5506=CARTESIAN_POINT('',(-0.32,0.,3.91886975727153E-17));
#5507=CARTESIAN_POINT('Origin',(0.,0.,0.));
#5508=CARTESIAN_POINT('Origin',(0.,0.,0.));
#5509=CARTESIAN_POINT('',(-0.6,0.16,7.34788079488412E-17));
#5510=CARTESIAN_POINT('Origin',(0.,0.16,0.));
#5511=CARTESIAN_POINT('',(-0.6,0.,7.34788079488412E-17));
#5512=CARTESIAN_POINT('',(-0.6,0.,7.34788079488412E-17));
#5513=CARTESIAN_POINT('Origin',(0.,0.,0.));
#5514=CARTESIAN_POINT('Origin',(0.,0.16,0.));
#5515=CARTESIAN_POINT('Origin',(0.,0.,0.));
#5619=UNCERTAINTY_MEASURE_WITH_UNIT(LENGTH_MEASURE(0.001),#5639,
'DISTANCE_ACCURACY_VALUE',
'Maximum model space distance between geometric entities at asserted c
onnectivities');
#5621=UNCERTAINTY_MEASURE_WITH_UNIT(LENGTH_MEASURE(0.001),#5639,
'DISTANCE_ACCURACY_VALUE',
'Maximum model space distance between geometric entities at asserted c
onnectivities');
#5636=(
GEOMETRIC_REPRESENTATION_CONTEXT(3)
GLOBAL_UNCERTAINTY_ASSIGNED_CONTEXT((#5619))
GLOBAL_UNIT_ASSIGNED_CONTEXT((#5639,#5641,#5642))
REPRESENTATION_CONTEXT('','3D')
);
#5638=(
GEOMETRIC_REPRESENTATION_CONTEXT(3)
GLOBAL_UNCERTAINTY_ASSIGNED_CONTEXT((#5621))
GLOBAL_UNIT_ASSIGNED_CONTEXT((#5639,#5641,#5642))
REPRESENTATION_CONTEXT('','3D')
);
#5639=(
LENGTH_UNIT()
NAMED_UNIT(*)
SI_UNIT(.CENTI.,.METRE.)
);
#5641=(
NAMED_UNIT(*)
PLANE_ANGLE_UNIT()
SI_UNIT($,.RADIAN.)
);
#5642=(
NAMED_UNIT(*)
SI_UNIT($,.STERADIAN.)
SOLID_ANGLE_UNIT()
);
#5657=SHAPE_DEFINITION_REPRESENTATION(#5675,#5714);
#5675=PRODUCT_DEFINITION_SHAPE('',$,#5731);
#5714=SHAPE_REPRESENTATION('',(#3623),#5636);
#5716=PRODUCT_DEFINITION_CONTEXT('part definition',#5766,'design');
#5731=PRODUCT_DEFINITION('Flat Washer - M6','Flat Washer - M6',
#5747,#5716);
#5747=PRODUCT_DEFINITION_FORMATION('',$,#5782);
#5766=APPLICATION_CONTEXT(
'Core Data for Automotive Mechanical Design Process');
#5767=PRODUCT_CONTEXT('part definition',#5766,'mechanical');
#5782=PRODUCT('Flat Washer - M6','Flat Washer - M6',
'Flat Washer - M6',(#5767));
#5861=COLOUR_RGB('Black',0.12,0.14,0.17);
#5862=FILL_AREA_STYLE_COLOUR('',#5861);
#5863=FILL_AREA_STYLE('',(#5862));
#5864=SURFACE_STYLE_FILL_AREA(#5863);
#5865=SURFACE_SIDE_STYLE('',(#5864));
#5866=SURFACE_STYLE_USAGE(.BOTH.,#5865);
#5867=PRESENTATION_STYLE_ASSIGNMENT((#5866));
ENDSEC;
END-ISO-10303-21;
